ISO-10303-21;
HEADER;
/* Generated by software containing ST-Developer
 * from STEP Tools, Inc. (www.steptools.com) 
 */

FILE_DESCRIPTION(
/* description */ (''),
/* implementation_level */ '2;1');

FILE_NAME(
/* name */ '09_Dust_Cap_1.98.step',
/* time_stamp */ '2026-10-25T01:26:34-07:00',
/* author */ (''),
/* organization */ (''),
/* preprocessor_version */ 'ST-DEVELOPER v20.2',
/* originating_system */ 'Autodesk Translation Framework v15.15.0.0',
/* authorisation */ '');

FILE_SCHEMA (('AUTOMOTIVE_DESIGN { 1 0 10303 214 3 1 1 }'));
ENDSEC;

DATA;
#10=MECHANICAL_DESIGN_GEOMETRIC_PRESENTATION_REPRESENTATION('',(#331),#71628);
#305=SHAPE_REPRESENTATION_RELATIONSHIP('SRR','None',#71693,#318);
#318=ADVANCED_BREP_SHAPE_REPRESENTATION('',(#344),#71625);
#331=STYLED_ITEM('',(#71832),#344);
#344=MANIFOLD_SOLID_BREP('Body1',#34218);
#1294=FACE_BOUND('',#7208,.T.);
#1295=FACE_BOUND('',#7212,.T.);
#2801=PLANE('',#37243);
#2802=PLANE('',#37250);
#2803=PLANE('',#37255);
#2804=PLANE('',#37256);
#3072=CYLINDRICAL_SURFACE('',#37241,25.6);
#3073=CYLINDRICAL_SURFACE('',#37248,25.12);
#3074=CYLINDRICAL_SURFACE('',#37252,26.8);
#3075=CYLINDRICAL_SURFACE('',#37268,24.32);
#4939=FACE_OUTER_BOUND('',#7198,.T.);
#4940=FACE_OUTER_BOUND('',#7199,.T.);
#4941=FACE_OUTER_BOUND('',#7200,.T.);
#4942=FACE_OUTER_BOUND('',#7201,.T.);
#4943=FACE_OUTER_BOUND('',#7202,.T.);
#4944=FACE_OUTER_BOUND('',#7203,.T.);
#4945=FACE_OUTER_BOUND('',#7204,.T.);
#4946=FACE_OUTER_BOUND('',#7205,.T.);
#4947=FACE_OUTER_BOUND('',#7206,.T.);
#4948=FACE_OUTER_BOUND('',#7207,.T.);
#4949=FACE_OUTER_BOUND('',#7209,.T.);
#4950=FACE_OUTER_BOUND('',#7210,.T.);
#4951=FACE_OUTER_BOUND('',#7211,.T.);
#4952=FACE_OUTER_BOUND('',#7213,.T.);
#4953=FACE_OUTER_BOUND('',#7214,.T.);
#4954=FACE_OUTER_BOUND('',#7215,.T.);
#4955=FACE_OUTER_BOUND('',#7216,.T.);
#4956=FACE_OUTER_BOUND('',#7217,.T.);
#4957=FACE_OUTER_BOUND('',#7218,.T.);
#4958=FACE_OUTER_BOUND('',#7219,.T.);
#4959=FACE_OUTER_BOUND('',#7220,.T.);
#4960=FACE_OUTER_BOUND('',#7221,.T.);
#4961=FACE_OUTER_BOUND('',#7222,.T.);
#7198=EDGE_LOOP('',(#30526,#30527,#30528,#30529,#30530,#30531));
#7199=EDGE_LOOP('',(#30532,#30533,#30534,#30535,#30536,#30537));
#7200=EDGE_LOOP('',(#30538,#30539,#30540,#30541,#30542));
#7201=EDGE_LOOP('',(#30543,#30544,#30545,#30546,#30547,#30548));
#7202=EDGE_LOOP('',(#30549,#30550,#30551,#30552,#30553,#30554));
#7203=EDGE_LOOP('',(#30555,#30556,#30557,#30558,#30559,#30560));
#7204=EDGE_LOOP('',(#30561,#30562,#30563,#30564,#30565,#30566));
#7205=EDGE_LOOP('',(#30567,#30568,#30569,#30570,#30571,#30572));
#7206=EDGE_LOOP('',(#30573,#30574,#30575,#30576,#30577));
#7207=EDGE_LOOP('',(#30578));
#7208=EDGE_LOOP('',(#30579));
#7209=EDGE_LOOP('',(#30580,#30581,#30582,#30583));
#7210=EDGE_LOOP('',(#30584,#30585,#30586,#30587));
#7211=EDGE_LOOP('',(#30588));
#7212=EDGE_LOOP('',(#30589));
#7213=EDGE_LOOP('',(#30590,#30591,#30592,#30593));
#7214=EDGE_LOOP('',(#30594,#30595,#30596,#30597));
#7215=EDGE_LOOP('',(#30598));
#7216=EDGE_LOOP('',(#30599));
#7217=EDGE_LOOP('',(#30600,#30601,#30602,#30603));
#7218=EDGE_LOOP('',(#30604,#30605,#30606,#30607));
#7219=EDGE_LOOP('',(#30608,#30609,#30610,#30611));
#7220=EDGE_LOOP('',(#30612,#30613,#30614,#30615));
#7221=EDGE_LOOP('',(#30616,#30617,#30618,#30619));
#7222=EDGE_LOOP('',(#30620,#30621,#30622,#30623));
#10186=LINE('',#62997,#13236);
#10187=LINE('',#63003,#13237);
#10188=LINE('',#63010,#13238);
#10189=LINE('',#63013,#13239);
#10190=LINE('',#63019,#13240);
#10191=LINE('',#63025,#13241);
#10192=LINE('',#63031,#13242);
#10193=LINE('',#63037,#13243);
#10194=LINE('',#63043,#13244);
#10195=LINE('',#63053,#13245);
#10196=LINE('',#63057,#13246);
#10197=LINE('',#63064,#13247);
#10198=LINE('',#63066,#13248);
#10199=LINE('',#63073,#13249);
#10200=LINE('',#63077,#13250);
#10201=LINE('',#63081,#13251);
#10202=LINE('',#63085,#13252);
#10203=LINE('',#63089,#13253);
#10204=LINE('',#63092,#13254);
#13236=VECTOR('',#46021,20.9831675294297);
#13237=VECTOR('',#46028,22.1);
#13238=VECTOR('',#46037,19.75);
#13239=VECTOR('',#46040,23.1453899562452);
#13240=VECTOR('',#46047,24.);
#13241=VECTOR('',#46054,24.7086590704751);
#13242=VECTOR('',#46061,25.2);
#13243=VECTOR('',#46068,25.5145642342283);
#13244=VECTOR('',#46075,25.6);
#13245=VECTOR('',#46088,24.82);
#13246=VECTOR('',#46093,25.12);
#13247=VECTOR('',#46102,26.8);
#13248=VECTOR('',#46105,26.2);
#13249=VECTOR('',#46114,19.55);
#13250=VECTOR('',#46119,21.65);
#13251=VECTOR('',#46124,23.3);
#13252=VECTOR('',#46129,24.4);
#13253=VECTOR('',#46134,24.56);
#13254=VECTOR('',#46139,24.32);
#14397=CIRCLE('',#37217,20.5035615807565);
#14398=CIRCLE('',#37218,20.5035615807565);
#14399=CIRCLE('',#37219,21.4627734781028);
#14400=CIRCLE('',#37220,21.4627734781028);
#14401=CIRCLE('',#37222,22.7372265218972);
#14402=CIRCLE('',#37223,22.7372265218972);
#14403=CIRCLE('',#37225,18.5);
#14404=CIRCLE('',#37227,23.5535533905933);
#14405=CIRCLE('',#37228,23.5535533905933);
#14406=CIRCLE('',#37230,24.4464466094067);
#14407=CIRCLE('',#37231,24.4464466094067);
#14408=CIRCLE('',#37233,24.9708715315434);
#14409=CIRCLE('',#37234,24.9708715315434);
#14410=CIRCLE('',#37236,25.4291284684566);
#14411=CIRCLE('',#37237,25.4291284684566);
#14412=CIRCLE('',#37239,25.6);
#14413=CIRCLE('',#37240,25.6);
#14414=CIRCLE('',#37242,25.6);
#14415=CIRCLE('',#37244,24.52);
#14416=CIRCLE('',#37245,24.32);
#14417=CIRCLE('',#37247,25.12);
#14418=CIRCLE('',#37249,25.12);
#14419=CIRCLE('',#37251,26.8);
#14420=CIRCLE('',#37253,26.8);
#14421=CIRCLE('',#37257,18.4);
#14422=CIRCLE('',#37259,20.7);
#14423=CIRCLE('',#37261,22.6);
#14424=CIRCLE('',#37263,24.);
#14425=CIRCLE('',#37265,24.8);
#14426=CIRCLE('',#37267,24.32);
#17002=VERTEX_POINT('',#62992);
#17003=VERTEX_POINT('',#62993);
#17004=VERTEX_POINT('',#62996);
#17005=VERTEX_POINT('',#62998);
#17006=VERTEX_POINT('',#63002);
#17007=VERTEX_POINT('',#63004);
#17008=VERTEX_POINT('',#63008);
#17009=VERTEX_POINT('',#63012);
#17010=VERTEX_POINT('',#63014);
#17011=VERTEX_POINT('',#63018);
#17012=VERTEX_POINT('',#63020);
#17013=VERTEX_POINT('',#63024);
#17014=VERTEX_POINT('',#63026);
#17015=VERTEX_POINT('',#63030);
#17016=VERTEX_POINT('',#63032);
#17017=VERTEX_POINT('',#63036);
#17018=VERTEX_POINT('',#63038);
#17019=VERTEX_POINT('',#63042);
#17020=VERTEX_POINT('',#63046);
#17021=VERTEX_POINT('',#63048);
#17022=VERTEX_POINT('',#63051);
#17023=VERTEX_POINT('',#63055);
#17024=VERTEX_POINT('',#63059);
#17025=VERTEX_POINT('',#63062);
#17026=VERTEX_POINT('',#63069);
#17027=VERTEX_POINT('',#63072);
#17028=VERTEX_POINT('',#63076);
#17029=VERTEX_POINT('',#63080);
#17030=VERTEX_POINT('',#63084);
#17031=VERTEX_POINT('',#63088);
#21577=EDGE_CURVE('',#17002,#17003,#14397,.T.);
#21578=EDGE_CURVE('',#17003,#17002,#14398,.T.);
#21579=EDGE_CURVE('',#17002,#17004,#10186,.T.);
#21580=EDGE_CURVE('',#17004,#17005,#14399,.T.);
#21581=EDGE_CURVE('',#17005,#17004,#14400,.T.);
#21582=EDGE_CURVE('',#17005,#17006,#10187,.T.);
#21583=EDGE_CURVE('',#17007,#17006,#14401,.T.);
#21584=EDGE_CURVE('',#17006,#17007,#14402,.T.);
#21585=EDGE_CURVE('',#17008,#17008,#14403,.T.);
#21586=EDGE_CURVE('',#17008,#17003,#10188,.T.);
#21587=EDGE_CURVE('',#17007,#17009,#10189,.T.);
#21588=EDGE_CURVE('',#17009,#17010,#14404,.T.);
#21589=EDGE_CURVE('',#17010,#17009,#14405,.T.);
#21590=EDGE_CURVE('',#17010,#17011,#10190,.T.);
#21591=EDGE_CURVE('',#17012,#17011,#14406,.T.);
#21592=EDGE_CURVE('',#17011,#17012,#14407,.T.);
#21593=EDGE_CURVE('',#17012,#17013,#10191,.T.);
#21594=EDGE_CURVE('',#17013,#17014,#14408,.T.);
#21595=EDGE_CURVE('',#17014,#17013,#14409,.T.);
#21596=EDGE_CURVE('',#17014,#17015,#10192,.T.);
#21597=EDGE_CURVE('',#17016,#17015,#14410,.T.);
#21598=EDGE_CURVE('',#17015,#17016,#14411,.T.);
#21599=EDGE_CURVE('',#17016,#17017,#10193,.T.);
#21600=EDGE_CURVE('',#17017,#17018,#14412,.T.);
#21601=EDGE_CURVE('',#17018,#17017,#14413,.T.);
#21602=EDGE_CURVE('',#17018,#17019,#10194,.T.);
#21603=EDGE_CURVE('',#17019,#17019,#14414,.T.);
#21604=EDGE_CURVE('',#17020,#17020,#14415,.T.);
#21605=EDGE_CURVE('',#17021,#17021,#14416,.T.);
#21606=EDGE_CURVE('',#17022,#17022,#14417,.T.);
#21607=EDGE_CURVE('',#17022,#17020,#10195,.T.);
#21608=EDGE_CURVE('',#17023,#17023,#14418,.T.);
#21609=EDGE_CURVE('',#17023,#17022,#10196,.T.);
#21610=EDGE_CURVE('',#17024,#17024,#14419,.T.);
#21611=EDGE_CURVE('',#17025,#17025,#14420,.T.);
#21612=EDGE_CURVE('',#17025,#17024,#10197,.T.);
#21613=EDGE_CURVE('',#17019,#17025,#10198,.T.);
#21614=EDGE_CURVE('',#17026,#17026,#14421,.T.);
#21615=EDGE_CURVE('',#17026,#17027,#10199,.T.);
#21616=EDGE_CURVE('',#17027,#17027,#14422,.T.);
#21617=EDGE_CURVE('',#17027,#17028,#10200,.T.);
#21618=EDGE_CURVE('',#17028,#17028,#14423,.T.);
#21619=EDGE_CURVE('',#17028,#17029,#10201,.T.);
#21620=EDGE_CURVE('',#17029,#17029,#14424,.T.);
#21621=EDGE_CURVE('',#17029,#17030,#10202,.T.);
#21622=EDGE_CURVE('',#17030,#17030,#14425,.T.);
#21623=EDGE_CURVE('',#17030,#17031,#10203,.T.);
#21624=EDGE_CURVE('',#17031,#17031,#14426,.T.);
#21625=EDGE_CURVE('',#17031,#17021,#10204,.T.);
#30526=ORIENTED_EDGE('',*,*,#21577,.T.);
#30527=ORIENTED_EDGE('',*,*,#21578,.T.);
#30528=ORIENTED_EDGE('',*,*,#21579,.T.);
#30529=ORIENTED_EDGE('',*,*,#21580,.T.);
#30530=ORIENTED_EDGE('',*,*,#21581,.T.);
#30531=ORIENTED_EDGE('',*,*,#21579,.F.);
#30532=ORIENTED_EDGE('',*,*,#21580,.F.);
#30533=ORIENTED_EDGE('',*,*,#21581,.F.);
#30534=ORIENTED_EDGE('',*,*,#21582,.T.);
#30535=ORIENTED_EDGE('',*,*,#21583,.F.);
#30536=ORIENTED_EDGE('',*,*,#21584,.F.);
#30537=ORIENTED_EDGE('',*,*,#21582,.F.);
#30538=ORIENTED_EDGE('',*,*,#21585,.F.);
#30539=ORIENTED_EDGE('',*,*,#21586,.T.);
#30540=ORIENTED_EDGE('',*,*,#21577,.F.);
#30541=ORIENTED_EDGE('',*,*,#21578,.F.);
#30542=ORIENTED_EDGE('',*,*,#21586,.F.);
#30543=ORIENTED_EDGE('',*,*,#21583,.T.);
#30544=ORIENTED_EDGE('',*,*,#21584,.T.);
#30545=ORIENTED_EDGE('',*,*,#21587,.T.);
#30546=ORIENTED_EDGE('',*,*,#21588,.T.);
#30547=ORIENTED_EDGE('',*,*,#21589,.T.);
#30548=ORIENTED_EDGE('',*,*,#21587,.F.);
#30549=ORIENTED_EDGE('',*,*,#21588,.F.);
#30550=ORIENTED_EDGE('',*,*,#21589,.F.);
#30551=ORIENTED_EDGE('',*,*,#21590,.T.);
#30552=ORIENTED_EDGE('',*,*,#21591,.F.);
#30553=ORIENTED_EDGE('',*,*,#21592,.F.);
#30554=ORIENTED_EDGE('',*,*,#21590,.F.);
#30555=ORIENTED_EDGE('',*,*,#21591,.T.);
#30556=ORIENTED_EDGE('',*,*,#21592,.T.);
#30557=ORIENTED_EDGE('',*,*,#21593,.T.);
#30558=ORIENTED_EDGE('',*,*,#21594,.T.);
#30559=ORIENTED_EDGE('',*,*,#21595,.T.);
#30560=ORIENTED_EDGE('',*,*,#21593,.F.);
#30561=ORIENTED_EDGE('',*,*,#21594,.F.);
#30562=ORIENTED_EDGE('',*,*,#21595,.F.);
#30563=ORIENTED_EDGE('',*,*,#21596,.T.);
#30564=ORIENTED_EDGE('',*,*,#21597,.F.);
#30565=ORIENTED_EDGE('',*,*,#21598,.F.);
#30566=ORIENTED_EDGE('',*,*,#21596,.F.);
#30567=ORIENTED_EDGE('',*,*,#21597,.T.);
#30568=ORIENTED_EDGE('',*,*,#21598,.T.);
#30569=ORIENTED_EDGE('',*,*,#21599,.T.);
#30570=ORIENTED_EDGE('',*,*,#21600,.T.);
#30571=ORIENTED_EDGE('',*,*,#21601,.T.);
#30572=ORIENTED_EDGE('',*,*,#21599,.F.);
#30573=ORIENTED_EDGE('',*,*,#21600,.F.);
#30574=ORIENTED_EDGE('',*,*,#21601,.F.);
#30575=ORIENTED_EDGE('',*,*,#21602,.T.);
#30576=ORIENTED_EDGE('',*,*,#21603,.T.);
#30577=ORIENTED_EDGE('',*,*,#21602,.F.);
#30578=ORIENTED_EDGE('',*,*,#21604,.F.);
#30579=ORIENTED_EDGE('',*,*,#21605,.T.);
#30580=ORIENTED_EDGE('',*,*,#21606,.F.);
#30581=ORIENTED_EDGE('',*,*,#21607,.T.);
#30582=ORIENTED_EDGE('',*,*,#21604,.T.);
#30583=ORIENTED_EDGE('',*,*,#21607,.F.);
#30584=ORIENTED_EDGE('',*,*,#21608,.F.);
#30585=ORIENTED_EDGE('',*,*,#21609,.T.);
#30586=ORIENTED_EDGE('',*,*,#21606,.T.);
#30587=ORIENTED_EDGE('',*,*,#21609,.F.);
#30588=ORIENTED_EDGE('',*,*,#21610,.F.);
#30589=ORIENTED_EDGE('',*,*,#21608,.T.);
#30590=ORIENTED_EDGE('',*,*,#21611,.F.);
#30591=ORIENTED_EDGE('',*,*,#21612,.T.);
#30592=ORIENTED_EDGE('',*,*,#21610,.T.);
#30593=ORIENTED_EDGE('',*,*,#21612,.F.);
#30594=ORIENTED_EDGE('',*,*,#21603,.F.);
#30595=ORIENTED_EDGE('',*,*,#21613,.T.);
#30596=ORIENTED_EDGE('',*,*,#21611,.T.);
#30597=ORIENTED_EDGE('',*,*,#21613,.F.);
#30598=ORIENTED_EDGE('',*,*,#21585,.T.);
#30599=ORIENTED_EDGE('',*,*,#21614,.F.);
#30600=ORIENTED_EDGE('',*,*,#21614,.T.);
#30601=ORIENTED_EDGE('',*,*,#21615,.T.);
#30602=ORIENTED_EDGE('',*,*,#21616,.F.);
#30603=ORIENTED_EDGE('',*,*,#21615,.F.);
#30604=ORIENTED_EDGE('',*,*,#21616,.T.);
#30605=ORIENTED_EDGE('',*,*,#21617,.T.);
#30606=ORIENTED_EDGE('',*,*,#21618,.F.);
#30607=ORIENTED_EDGE('',*,*,#21617,.F.);
#30608=ORIENTED_EDGE('',*,*,#21618,.T.);
#30609=ORIENTED_EDGE('',*,*,#21619,.T.);
#30610=ORIENTED_EDGE('',*,*,#21620,.F.);
#30611=ORIENTED_EDGE('',*,*,#21619,.F.);
#30612=ORIENTED_EDGE('',*,*,#21620,.T.);
#30613=ORIENTED_EDGE('',*,*,#21621,.T.);
#30614=ORIENTED_EDGE('',*,*,#21622,.F.);
#30615=ORIENTED_EDGE('',*,*,#21621,.F.);
#30616=ORIENTED_EDGE('',*,*,#21622,.T.);
#30617=ORIENTED_EDGE('',*,*,#21623,.T.);
#30618=ORIENTED_EDGE('',*,*,#21624,.F.);
#30619=ORIENTED_EDGE('',*,*,#21623,.F.);
#30620=ORIENTED_EDGE('',*,*,#21624,.T.);
#30621=ORIENTED_EDGE('',*,*,#21625,.T.);
#30622=ORIENTED_EDGE('',*,*,#21605,.F.);
#30623=ORIENTED_EDGE('',*,*,#21625,.F.);
#32084=CONICAL_SURFACE('',#37216,20.9831675294297,1.3169225046995);
#32085=CONICAL_SURFACE('',#37221,22.1,1.18247760862243);
#32086=CONICAL_SURFACE('',#37224,19.75,1.45136740077656);
#32087=CONICAL_SURFACE('',#37226,23.1453899562452,0.98393788600994);
#32088=CONICAL_SURFACE('',#37229,24.,0.785398163397448);
#32089=CONICAL_SURFACE('',#37232,24.708659070475,0.567084583490677);
#32090=CONICAL_SURFACE('',#37235,25.2,0.348771003583908);
#32091=CONICAL_SURFACE('',#37238,25.5145642342283,0.174385501791952);
#32092=CONICAL_SURFACE('',#37246,24.82,0.785398163397448);
#32093=CONICAL_SURFACE('',#37254,26.2,1.24904577239825);
#32094=CONICAL_SURFACE('',#37258,19.55,1.44109378963898);
#32095=CONICAL_SURFACE('',#37260,21.65,1.17227388112848);
#32096=CONICAL_SURFACE('',#37262,23.3,0.750929062397939);
#32097=CONICAL_SURFACE('',#37264,24.4,0.41822432957923);
#32098=CONICAL_SURFACE('',#37266,24.56,0.0263675140393565);
#33913=ADVANCED_FACE('',(#4939),#32084,.T.);
#33914=ADVANCED_FACE('',(#4940),#32085,.T.);
#33915=ADVANCED_FACE('',(#4941),#32086,.T.);
#33916=ADVANCED_FACE('',(#4942),#32087,.T.);
#33917=ADVANCED_FACE('',(#4943),#32088,.T.);
#33918=ADVANCED_FACE('',(#4944),#32089,.T.);
#33919=ADVANCED_FACE('',(#4945),#32090,.T.);
#33920=ADVANCED_FACE('',(#4946),#32091,.T.);
#33921=ADVANCED_FACE('',(#4947),#3072,.T.);
#33922=ADVANCED_FACE('',(#4948,#1294),#2801,.T.);
#33923=ADVANCED_FACE('',(#4949),#32092,.T.);
#33924=ADVANCED_FACE('',(#4950),#3073,.T.);
#33925=ADVANCED_FACE('',(#4951,#1295),#2802,.T.);
#33926=ADVANCED_FACE('',(#4952),#3074,.T.);
#33927=ADVANCED_FACE('',(#4953),#32093,.T.);
#33928=ADVANCED_FACE('',(#4954),#2803,.T.);
#33929=ADVANCED_FACE('',(#4955),#2804,.T.);
#33930=ADVANCED_FACE('',(#4956),#32094,.F.);
#33931=ADVANCED_FACE('',(#4957),#32095,.F.);
#33932=ADVANCED_FACE('',(#4958),#32096,.F.);
#33933=ADVANCED_FACE('',(#4959),#32097,.F.);
#33934=ADVANCED_FACE('',(#4960),#32098,.F.);
#33935=ADVANCED_FACE('',(#4961),#3075,.F.);
#34218=CLOSED_SHELL('',(#33913,#33914,#33915,#33916,#33917,#33918,#33919,
#33920,#33921,#33922,#33923,#33924,#33925,#33926,#33927,#33928,#33929,#33930,
#33931,#33932,#33933,#33934,#33935));
#37215=AXIS2_PLACEMENT_3D('',#62990,#46013,#46014);
#37216=AXIS2_PLACEMENT_3D('',#62991,#46015,#46016);
#37217=AXIS2_PLACEMENT_3D('',#62994,#46017,#46018);
#37218=AXIS2_PLACEMENT_3D('',#62995,#46019,#46020);
#37219=AXIS2_PLACEMENT_3D('',#62999,#46022,#46023);
#37220=AXIS2_PLACEMENT_3D('',#63000,#46024,#46025);
#37221=AXIS2_PLACEMENT_3D('',#63001,#46026,#46027);
#37222=AXIS2_PLACEMENT_3D('',#63005,#46029,#46030);
#37223=AXIS2_PLACEMENT_3D('',#63006,#46031,#46032);
#37224=AXIS2_PLACEMENT_3D('',#63007,#46033,#46034);
#37225=AXIS2_PLACEMENT_3D('',#63009,#46035,#46036);
#37226=AXIS2_PLACEMENT_3D('',#63011,#46038,#46039);
#37227=AXIS2_PLACEMENT_3D('',#63015,#46041,#46042);
#37228=AXIS2_PLACEMENT_3D('',#63016,#46043,#46044);
#37229=AXIS2_PLACEMENT_3D('',#63017,#46045,#46046);
#37230=AXIS2_PLACEMENT_3D('',#63021,#46048,#46049);
#37231=AXIS2_PLACEMENT_3D('',#63022,#46050,#46051);
#37232=AXIS2_PLACEMENT_3D('',#63023,#46052,#46053);
#37233=AXIS2_PLACEMENT_3D('',#63027,#46055,#46056);
#37234=AXIS2_PLACEMENT_3D('',#63028,#46057,#46058);
#37235=AXIS2_PLACEMENT_3D('',#63029,#46059,#46060);
#37236=AXIS2_PLACEMENT_3D('',#63033,#46062,#46063);
#37237=AXIS2_PLACEMENT_3D('',#63034,#46064,#46065);
#37238=AXIS2_PLACEMENT_3D('',#63035,#46066,#46067);
#37239=AXIS2_PLACEMENT_3D('',#63039,#46069,#46070);
#37240=AXIS2_PLACEMENT_3D('',#63040,#46071,#46072);
#37241=AXIS2_PLACEMENT_3D('',#63041,#46073,#46074);
#37242=AXIS2_PLACEMENT_3D('',#63044,#46076,#46077);
#37243=AXIS2_PLACEMENT_3D('',#63045,#46078,#46079);
#37244=AXIS2_PLACEMENT_3D('',#63047,#46080,#46081);
#37245=AXIS2_PLACEMENT_3D('',#63049,#46082,#46083);
#37246=AXIS2_PLACEMENT_3D('',#63050,#46084,#46085);
#37247=AXIS2_PLACEMENT_3D('',#63052,#46086,#46087);
#37248=AXIS2_PLACEMENT_3D('',#63054,#46089,#46090);
#37249=AXIS2_PLACEMENT_3D('',#63056,#46091,#46092);
#37250=AXIS2_PLACEMENT_3D('',#63058,#46094,#46095);
#37251=AXIS2_PLACEMENT_3D('',#63060,#46096,#46097);
#37252=AXIS2_PLACEMENT_3D('',#63061,#46098,#46099);
#37253=AXIS2_PLACEMENT_3D('',#63063,#46100,#46101);
#37254=AXIS2_PLACEMENT_3D('',#63065,#46103,#46104);
#37255=AXIS2_PLACEMENT_3D('',#63067,#46106,#46107);
#37256=AXIS2_PLACEMENT_3D('',#63068,#46108,#46109);
#37257=AXIS2_PLACEMENT_3D('',#63070,#46110,#46111);
#37258=AXIS2_PLACEMENT_3D('',#63071,#46112,#46113);
#37259=AXIS2_PLACEMENT_3D('',#63074,#46115,#46116);
#37260=AXIS2_PLACEMENT_3D('',#63075,#46117,#46118);
#37261=AXIS2_PLACEMENT_3D('',#63078,#46120,#46121);
#37262=AXIS2_PLACEMENT_3D('',#63079,#46122,#46123);
#37263=AXIS2_PLACEMENT_3D('',#63082,#46125,#46126);
#37264=AXIS2_PLACEMENT_3D('',#63083,#46127,#46128);
#37265=AXIS2_PLACEMENT_3D('',#63086,#46130,#46131);
#37266=AXIS2_PLACEMENT_3D('',#63087,#46132,#46133);
#37267=AXIS2_PLACEMENT_3D('',#63090,#46135,#46136);
#37268=AXIS2_PLACEMENT_3D('',#63091,#46137,#46138);
#46013=DIRECTION('axis',(0.,0.,1.));
#46014=DIRECTION('refdir',(1.,0.,0.));
#46015=DIRECTION('center_axis',(-1.,0.,-2.35987854673648E-16));
#46016=DIRECTION('ref_axis',(0.,-1.,-6.12323399573677E-17));
#46017=DIRECTION('center_axis',(-1.,0.,0.));
#46018=DIRECTION('ref_axis',(0.,-1.,-6.12323399573677E-17));
#46019=DIRECTION('center_axis',(-1.,0.,0.));
#46020=DIRECTION('ref_axis',(0.,-1.,-6.12323399573677E-17));
#46021=DIRECTION('',(-0.251155487883568,0.967946755201941,1.18539289550312E-16));
#46022=DIRECTION('center_axis',(1.,0.,0.));
#46023=DIRECTION('ref_axis',(0.,-1.,-6.12323399573677E-17));
#46024=DIRECTION('center_axis',(1.,0.,0.));
#46025=DIRECTION('ref_axis',(0.,-1.,-6.12323399573677E-17));
#46026=DIRECTION('center_axis',(-1.,0.,0.));
#46027=DIRECTION('ref_axis',(0.,1.,0.));
#46028=DIRECTION('',(-0.378632845720504,-0.925546956205677,-1.13346811737786E-16));
#46029=DIRECTION('center_axis',(-1.,0.,0.));
#46030=DIRECTION('ref_axis',(0.,-1.,-6.12323399573677E-17));
#46031=DIRECTION('center_axis',(-1.,0.,0.));
#46032=DIRECTION('ref_axis',(0.,-1.,-6.12323399573677E-17));
#46033=DIRECTION('center_axis',(-1.,0.,0.));
#46034=DIRECTION('ref_axis',(0.,1.,0.));
#46035=DIRECTION('center_axis',(1.,0.,0.));
#46036=DIRECTION('ref_axis',(0.,0.,-1.));
#46037=DIRECTION('',(-0.119145220618432,-0.992876838486922,-1.21592344220055E-16));
#46038=DIRECTION('center_axis',(-1.,0.,-9.20765957170186E-17));
#46039=DIRECTION('ref_axis',(0.,-1.,-6.12323399573676E-17));
#46040=DIRECTION('',(-0.553747832388229,0.832684416886336,1.01974430583973E-16));
#46041=DIRECTION('center_axis',(1.,0.,0.));
#46042=DIRECTION('ref_axis',(0.,-1.,-6.12323399573676E-17));
#46043=DIRECTION('center_axis',(1.,0.,0.));
#46044=DIRECTION('ref_axis',(0.,-1.,-6.12323399573676E-17));
#46045=DIRECTION('center_axis',(-1.,0.,0.));
#46046=DIRECTION('ref_axis',(0.,1.,0.));
#46047=DIRECTION('',(-0.707106781186548,-0.707106781186548,-8.65956056235494E-17));
#46048=DIRECTION('center_axis',(-1.,0.,0.));
#46049=DIRECTION('ref_axis',(0.,-1.,-6.12323399573677E-17));
#46050=DIRECTION('center_axis',(-1.,0.,0.));
#46051=DIRECTION('ref_axis',(0.,-1.,-6.12323399573677E-17));
#46052=DIRECTION('center_axis',(-1.,0.,-3.89966131806063E-17));
#46053=DIRECTION('ref_axis',(0.,-1.,-6.12323399573677E-17));
#46054=DIRECTION('',(-0.843470647186707,0.537175266867749,6.57849971150714E-17));
#46055=DIRECTION('center_axis',(1.,0.,0.));
#46056=DIRECTION('ref_axis',(0.,-1.,-6.12323399573676E-17));
#46057=DIRECTION('center_axis',(1.,0.,0.));
#46058=DIRECTION('ref_axis',(0.,-1.,-6.12323399573676E-17));
#46059=DIRECTION('center_axis',(-1.,0.,0.));
#46060=DIRECTION('ref_axis',(0.,1.,0.));
#46061=DIRECTION('',(-0.939793423488437,-0.341743063086705,-4.18514548339945E-17));
#46062=DIRECTION('center_axis',(-1.,0.,0.));
#46063=DIRECTION('ref_axis',(0.,-1.,-6.12323399573677E-17));
#46064=DIRECTION('center_axis',(-1.,0.,0.));
#46065=DIRECTION('ref_axis',(0.,-1.,-6.12323399573677E-17));
#46066=DIRECTION('center_axis',(-1.,0.,1.60541325725285E-15));
#46067=DIRECTION('ref_axis',(0.,-1.,-3.05136514366029E-17));
#46068=DIRECTION('',(-0.984833342116431,0.173502992065788,1.60760670182904E-15));
#46069=DIRECTION('center_axis',(1.,0.,0.));
#46070=DIRECTION('ref_axis',(0.,-1.,0.));
#46071=DIRECTION('center_axis',(1.,0.,0.));
#46072=DIRECTION('ref_axis',(0.,-1.,0.));
#46073=DIRECTION('center_axis',(1.,0.,0.));
#46074=DIRECTION('ref_axis',(0.,1.,0.));
#46075=DIRECTION('',(-1.,0.,0.));
#46076=DIRECTION('center_axis',(1.,0.,0.));
#46077=DIRECTION('ref_axis',(0.,0.,-1.));
#46078=DIRECTION('center_axis',(-1.,0.,0.));
#46079=DIRECTION('ref_axis',(0.,0.,1.));
#46080=DIRECTION('center_axis',(1.,0.,0.));
#46081=DIRECTION('ref_axis',(0.,0.,-1.));
#46082=DIRECTION('center_axis',(1.,0.,0.));
#46083=DIRECTION('ref_axis',(0.,0.,-1.));
#46084=DIRECTION('center_axis',(1.,0.,0.));
#46085=DIRECTION('ref_axis',(0.,1.,0.));
#46086=DIRECTION('center_axis',(1.,0.,0.));
#46087=DIRECTION('ref_axis',(0.,0.,-1.));
#46088=DIRECTION('',(-0.707106781186547,0.707106781186547,8.65956056235493E-17));
#46089=DIRECTION('center_axis',(1.,0.,0.));
#46090=DIRECTION('ref_axis',(0.,1.,0.));
#46091=DIRECTION('center_axis',(1.,0.,0.));
#46092=DIRECTION('ref_axis',(0.,0.,-1.));
#46093=DIRECTION('',(-1.,0.,0.));
#46094=DIRECTION('center_axis',(-1.,0.,0.));
#46095=DIRECTION('ref_axis',(0.,0.,1.));
#46096=DIRECTION('center_axis',(1.,0.,0.));
#46097=DIRECTION('ref_axis',(0.,0.,-1.));
#46098=DIRECTION('center_axis',(1.,0.,0.));
#46099=DIRECTION('ref_axis',(0.,1.,0.));
#46100=DIRECTION('center_axis',(1.,0.,0.));
#46101=DIRECTION('ref_axis',(0.,0.,-1.));
#46102=DIRECTION('',(-1.,0.,0.));
#46103=DIRECTION('center_axis',(-1.,0.,0.));
#46104=DIRECTION('ref_axis',(0.,1.,0.));
#46105=DIRECTION('',(-0.316227766016838,-0.948683298050514,-1.16180196436212E-16));
#46106=DIRECTION('center_axis',(1.,0.,0.));
#46107=DIRECTION('ref_axis',(0.,0.,-1.));
#46108=DIRECTION('center_axis',(-1.,0.,0.));
#46109=DIRECTION('ref_axis',(0.,0.,1.));
#46110=DIRECTION('center_axis',(1.,0.,0.));
#46111=DIRECTION('ref_axis',(0.,0.,-1.));
#46112=DIRECTION('center_axis',(-1.,0.,0.));
#46113=DIRECTION('ref_axis',(0.,1.,0.));
#46114=DIRECTION('',(-0.129339184067768,-0.991600411186222,-1.21436026959241E-16));
#46115=DIRECTION('center_axis',(1.,0.,0.));
#46116=DIRECTION('ref_axis',(0.,0.,-1.));
#46117=DIRECTION('center_axis',(-1.,0.,0.));
#46118=DIRECTION('ref_axis',(0.,1.,0.));
#46119=DIRECTION('',(-0.388057000058132,-0.921635375138065,-1.1286778121438E-16));
#46120=DIRECTION('center_axis',(1.,0.,0.));
#46121=DIRECTION('ref_axis',(0.,0.,-1.));
#46122=DIRECTION('center_axis',(-1.,0.,0.));
#46123=DIRECTION('ref_axis',(0.,1.,0.));
#46124=DIRECTION('',(-0.73105526824287,-0.68231825036001,-8.35598861303209E-17));
#46125=DIRECTION('center_axis',(1.,0.,0.));
#46126=DIRECTION('ref_axis',(0.,0.,-1.));
#46127=DIRECTION('center_axis',(-1.,0.,0.));
#46128=DIRECTION('ref_axis',(0.,1.,0.));
#46129=DIRECTION('',(-0.913811548620257,-0.406138466053448,-4.97376172462971E-17));
#46130=DIRECTION('center_axis',(1.,0.,0.));
#46131=DIRECTION('ref_axis',(0.,0.,-1.));
#46132=DIRECTION('center_axis',(1.,0.,0.));
#46133=DIRECTION('ref_axis',(0.,1.,0.));
#46134=DIRECTION('',(-0.999652397241505,0.0263644588283474,3.22871501153878E-18));
#46135=DIRECTION('center_axis',(1.,0.,0.));
#46136=DIRECTION('ref_axis',(0.,0.,-1.));
#46137=DIRECTION('center_axis',(1.,0.,0.));
#46138=DIRECTION('ref_axis',(0.,1.,0.));
#46139=DIRECTION('',(-1.,0.,0.));
#62990=CARTESIAN_POINT('',(0.,0.,0.));
#62991=CARTESIAN_POINT('Origin',(15.6351280937245,0.,-1.28484844754444E-15));
#62992=CARTESIAN_POINT('',(15.7595726103092,20.5035615807565,-2.51096210609941E-15));
#62993=CARTESIAN_POINT('',(15.7595726103092,-20.5035615807565,-2.51096210609941E-15));
#62994=CARTESIAN_POINT('Origin',(15.7595726103092,0.,-1.25548105304971E-15));
#62995=CARTESIAN_POINT('Origin',(15.7595726103092,0.,-1.25548105304971E-15));
#62996=CARTESIAN_POINT('',(15.5106835771397,21.4627734781028,2.62843168407833E-15));
#62997=CARTESIAN_POINT('',(15.6351280937245,20.9831675294297,2.56969689508887E-15));
#62998=CARTESIAN_POINT('',(15.5106835771397,-21.4627734781028,-2.62843168407833E-15));
#62999=CARTESIAN_POINT('Origin',(15.5106835771397,0.,-1.31421584203917E-15));
#63000=CARTESIAN_POINT('Origin',(15.5106835771397,0.,-1.31421584203917E-15));
#63001=CARTESIAN_POINT('Origin',(15.25,0.,0.));
#63002=CARTESIAN_POINT('',(14.9893164228603,-22.7372265218972,-2.78450716815297E-15));
#63003=CARTESIAN_POINT('',(15.25,-22.1,-2.70646942611565E-15));
#63004=CARTESIAN_POINT('',(14.9893164228603,22.7372265218972,-2.78450716815297E-15));
#63005=CARTESIAN_POINT('Origin',(14.9893164228603,0.,-1.39225358407648E-15));
#63006=CARTESIAN_POINT('Origin',(14.9893164228603,0.,-1.39225358407648E-15));
#63007=CARTESIAN_POINT('Origin',(15.85,0.,0.));
#63008=CARTESIAN_POINT('',(16.,-18.5,-2.2655965784226E-15));
#63009=CARTESIAN_POINT('Origin',(16.,0.,0.));
#63010=CARTESIAN_POINT('',(15.85,-19.75,-2.41867742831602E-15));
#63011=CARTESIAN_POINT('Origin',(14.7178815161335,0.,-1.41724638624665E-15));
#63012=CARTESIAN_POINT('',(14.4464466094067,23.5535533905933,2.88447837683363E-15));
#63013=CARTESIAN_POINT('',(14.7178815161335,23.1453899562452,2.8344927724933E-15));
#63014=CARTESIAN_POINT('',(14.4464466094067,-23.5535533905933,-2.88447837683363E-15));
#63015=CARTESIAN_POINT('Origin',(14.4464466094067,0.,-1.44223918841682E-15));
#63016=CARTESIAN_POINT('Origin',(14.4464466094067,0.,-1.44223918841682E-15));
#63017=CARTESIAN_POINT('Origin',(14.,0.,0.));
#63018=CARTESIAN_POINT('',(13.5535533905933,-24.4464466094067,-2.99382625907366E-15));
#63019=CARTESIAN_POINT('',(14.,-24.,-2.93915231795365E-15));
#63020=CARTESIAN_POINT('',(13.5535533905933,24.4464466094067,-2.99382625907366E-15));
#63021=CARTESIAN_POINT('Origin',(13.5535533905933,0.,-1.49691312953683E-15));
#63022=CARTESIAN_POINT('Origin',(13.5535533905933,0.,-1.49691312953683E-15));
#63023=CARTESIAN_POINT('Origin',(13.1418283394245,0.,-1.51296901209402E-15));
#63024=CARTESIAN_POINT('',(12.7301032882558,24.9708715315434,3.05804978930243E-15));
#63025=CARTESIAN_POINT('',(13.1418283394245,24.708659070475,3.02593802418805E-15));
#63026=CARTESIAN_POINT('',(12.7301032882558,-24.9708715315434,-3.05804978930243E-15));
#63027=CARTESIAN_POINT('Origin',(12.7301032882558,0.,-1.52902489465122E-15));
#63028=CARTESIAN_POINT('Origin',(12.7301032882558,0.,-1.52902489465122E-15));
#63029=CARTESIAN_POINT('Origin',(12.1,0.,0.));
#63030=CARTESIAN_POINT('',(11.4698967117442,-25.4291284684566,-3.11417007840023E-15));
#63031=CARTESIAN_POINT('',(12.1,-25.2,-3.08610993385133E-15));
#63032=CARTESIAN_POINT('',(11.4698967117442,25.4291284684566,-3.11417007840023E-15));
#63033=CARTESIAN_POINT('Origin',(11.4698967117442,0.,-1.55708503920011E-15));
#63034=CARTESIAN_POINT('Origin',(11.4698967117442,0.,-1.55708503920011E-15));
#63035=CARTESIAN_POINT('Origin',(10.9849483558721,0.,-7.78542519600057E-16));
#63036=CARTESIAN_POINT('',(10.5,25.6,3.13509580581722E-15));
#63037=CARTESIAN_POINT('',(10.9849483558721,25.5145642342283,3.12463294210873E-15));
#63038=CARTESIAN_POINT('',(10.5,-25.6,-3.13509580581722E-15));
#63039=CARTESIAN_POINT('Origin',(10.5,0.,0.));
#63040=CARTESIAN_POINT('Origin',(10.5,0.,0.));
#63041=CARTESIAN_POINT('Origin',(6.3,0.,0.));
#63042=CARTESIAN_POINT('',(1.6,-25.6,-3.13509580581722E-15));
#63043=CARTESIAN_POINT('',(6.3,-25.6,-3.13509580581722E-15));
#63044=CARTESIAN_POINT('Origin',(1.6,0.,0.));
#63045=CARTESIAN_POINT('Origin',(-8.,24.52,0.));
#63046=CARTESIAN_POINT('',(-8.,-24.52,-3.00283395150931E-15));
#63047=CARTESIAN_POINT('Origin',(-8.,0.,0.));
#63048=CARTESIAN_POINT('',(-8.,-24.32,-2.97834101552636E-15));
#63049=CARTESIAN_POINT('Origin',(-8.,0.,0.));
#63050=CARTESIAN_POINT('Origin',(-7.7,0.,0.));
#63051=CARTESIAN_POINT('',(-7.4,-25.12,-3.07631275945815E-15));
#63052=CARTESIAN_POINT('Origin',(-7.4,0.,0.));
#63053=CARTESIAN_POINT('',(-7.7,-24.82,-3.03957335548373E-15));
#63054=CARTESIAN_POINT('Origin',(-3.7,0.,0.));
#63055=CARTESIAN_POINT('',(0.,-25.12,-3.07631275945815E-15));
#63056=CARTESIAN_POINT('Origin',(0.,0.,0.));
#63057=CARTESIAN_POINT('',(-3.7,-25.12,-3.07631275945815E-15));
#63058=CARTESIAN_POINT('Origin',(0.,26.8,0.));
#63059=CARTESIAN_POINT('',(0.,-26.8,-3.28205342171491E-15));
#63060=CARTESIAN_POINT('Origin',(0.,0.,0.));
#63061=CARTESIAN_POINT('Origin',(0.599999999999999,0.,0.));
#63062=CARTESIAN_POINT('',(1.2,-26.8,-3.28205342171491E-15));
#63063=CARTESIAN_POINT('Origin',(1.2,0.,0.));
#63064=CARTESIAN_POINT('',(0.599999999999999,-26.8,-3.28205342171491E-15));
#63065=CARTESIAN_POINT('Origin',(1.4,0.,0.));
#63066=CARTESIAN_POINT('',(1.4,-26.2,-3.20857461376607E-15));
#63067=CARTESIAN_POINT('Origin',(16.,0.,0.));
#63068=CARTESIAN_POINT('Origin',(15.2,18.4,0.));
#63069=CARTESIAN_POINT('',(15.2,-18.4,-2.25335011043113E-15));
#63070=CARTESIAN_POINT('Origin',(15.2,0.,0.));
#63071=CARTESIAN_POINT('Origin',(15.05,0.,0.));
#63072=CARTESIAN_POINT('',(14.9,-20.7,-2.53501887423502E-15));
#63073=CARTESIAN_POINT('',(15.05,-19.55,-2.39418449233308E-15));
#63074=CARTESIAN_POINT('Origin',(14.9,0.,0.));
#63075=CARTESIAN_POINT('Origin',(14.5,0.,0.));
#63076=CARTESIAN_POINT('',(14.1,-22.6,-2.76770176607302E-15));
#63077=CARTESIAN_POINT('',(14.5,-21.65,-2.65136032015402E-15));
#63078=CARTESIAN_POINT('Origin',(14.1,0.,0.));
#63079=CARTESIAN_POINT('Origin',(13.35,0.,0.));
#63080=CARTESIAN_POINT('',(12.6,-24.,-2.93915231795365E-15));
#63081=CARTESIAN_POINT('',(13.35,-23.3,-2.85342704201333E-15));
#63082=CARTESIAN_POINT('Origin',(12.6,0.,0.));
#63083=CARTESIAN_POINT('Origin',(11.7,0.,0.));
#63084=CARTESIAN_POINT('',(10.8,-24.8,-3.03712406188544E-15));
#63085=CARTESIAN_POINT('',(11.7,-24.4,-2.98813818991954E-15));
#63086=CARTESIAN_POINT('Origin',(10.8,0.,0.));
#63087=CARTESIAN_POINT('Origin',(1.7,0.,0.));
#63088=CARTESIAN_POINT('',(-7.4,-24.32,-2.97834101552636E-15));
#63089=CARTESIAN_POINT('',(1.7,-24.56,-3.0077325387059E-15));
#63090=CARTESIAN_POINT('Origin',(-7.4,0.,0.));
#63091=CARTESIAN_POINT('Origin',(-7.7,0.,0.));
#63092=CARTESIAN_POINT('',(-7.7,-24.32,-2.97834101552636E-15));
#71610=UNCERTAINTY_MEASURE_WITH_UNIT(LENGTH_MEASURE(0.01),#71629,
'DISTANCE_ACCURACY_VALUE',
'Maximum model space distance between geometric entities at asserted c
onnectivities');
#71613=UNCERTAINTY_MEASURE_WITH_UNIT(LENGTH_MEASURE(0.01),#71629,
'DISTANCE_ACCURACY_VALUE',
'Maximum model space distance between geometric entities at asserted c
onnectivities');
#71625=(
GEOMETRIC_REPRESENTATION_CONTEXT(3)
GLOBAL_UNCERTAINTY_ASSIGNED_CONTEXT((#71610))
GLOBAL_UNIT_ASSIGNED_CONTEXT((#71629,#71631,#71632))
REPRESENTATION_CONTEXT('','3D')
);
#71628=(
GEOMETRIC_REPRESENTATION_CONTEXT(3)
GLOBAL_UNCERTAINTY_ASSIGNED_CONTEXT((#71613))
GLOBAL_UNIT_ASSIGNED_CONTEXT((#71629,#71631,#71632))
REPRESENTATION_CONTEXT('','3D')
);
#71629=(
LENGTH_UNIT()
NAMED_UNIT(*)
SI_UNIT(.MILLI.,.METRE.)
);
#71631=(
NAMED_UNIT(*)
PLANE_ANGLE_UNIT()
SI_UNIT($,.RADIAN.)
);
#71632=(
NAMED_UNIT(*)
SI_UNIT($,.STERADIAN.)
SOLID_ANGLE_UNIT()
);
#71644=SHAPE_DEFINITION_REPRESENTATION(#71658,#71693);
#71658=PRODUCT_DEFINITION_SHAPE('',$,#71708);
#71693=SHAPE_REPRESENTATION('',(#37215),#71625);
#71696=PRODUCT_DEFINITION_CONTEXT('part definition',#71740,'design');
#71708=PRODUCT_DEFINITION('2026-10-25-00-23-52-521','09_Dust_Cap_1.98',
#71722,#71696);
#71722=PRODUCT_DEFINITION_FORMATION('',$,#71753);
#71740=APPLICATION_CONTEXT(
'Core Data for Automotive Mechanical Design Process');
#71741=PRODUCT_CONTEXT('part definition',#71740,'mechanical');
#71753=PRODUCT('2026-10-25-00-23-52-521','09_Dust_Cap_1.98',$,(#71741));
#71826=COLOUR_RGB('Off White',0.89,0.88,0.83);
#71827=FILL_AREA_STYLE_COLOUR('',#71826);
#71828=FILL_AREA_STYLE('',(#71827));
#71829=SURFACE_STYLE_FILL_AREA(#71828);
#71830=SURFACE_SIDE_STYLE('',(#71829));
#71831=SURFACE_STYLE_USAGE(.BOTH.,#71830);
#71832=PRESENTATION_STYLE_ASSIGNMENT((#71831));
ENDSEC;
END-ISO-10303-21;
